ISO-10303-21;
HEADER;
/* Generated by software containing ST-Developer
 * from STEP Tools, Inc. (www.steptools.com) 
 */

FILE_DESCRIPTION(
/* description */ (''),
/* implementation_level */ '2;1');

FILE_NAME(
/* name */ 'Pin_04.step',
/* time_stamp */ '2026-10-23T17:00:58+06:00',
/* author */ (''),
/* organization */ (''),
/* preprocessor_version */ 'ST-DEVELOPER v20.2',
/* originating_system */ 'Autodesk Translation Framework v15.15.0.0',
/* authorisation */ '');

FILE_SCHEMA (('AUTOMOTIVE_DESIGN { 1 0 10303 214 3 1 1 }'));
ENDSEC;

DATA;
#10=MECHANICAL_DESIGN_GEOMETRIC_PRESENTATION_REPRESENTATION('',(#111),#11385);
#85=SHAPE_REPRESENTATION_RELATIONSHIP('SRR','None',#11437,#98);
#98=ADVANCED_BREP_SHAPE_REPRESENTATION('',(#124),#11377);
#111=STYLED_ITEM('',(#11567),#124);
#124=MANIFOLD_SOLID_BREP('Pin_04',#5347);
#265=CONICAL_SURFACE('',#6005,0.7,0.785398163397451);
#266=CONICAL_SURFACE('',#6011,0.7,0.785398163397448);
#497=CIRCLE('',#6006,0.649999999999999);
#498=CIRCLE('',#6007,0.75);
#499=CIRCLE('',#6009,0.75);
#500=CIRCLE('',#6012,0.649999999999999);
#599=CYLINDRICAL_SURFACE('',#6008,0.75);
#880=FACE_OUTER_BOUND('',#1240,.T.);
#881=FACE_OUTER_BOUND('',#1241,.T.);
#882=FACE_OUTER_BOUND('',#1242,.T.);
#883=FACE_OUTER_BOUND('',#1243,.T.);
#884=FACE_OUTER_BOUND('',#1244,.T.);
#1240=EDGE_LOOP('',(#4680,#4681,#4682,#4683));
#1241=EDGE_LOOP('',(#4684,#4685,#4686,#4687));
#1242=EDGE_LOOP('',(#4688));
#1243=EDGE_LOOP('',(#4689,#4690,#4691,#4692));
#1244=EDGE_LOOP('',(#4693));
#1710=LINE('',#9645,#2172);
#1711=LINE('',#9649,#2173);
#1712=LINE('',#9654,#2174);
#2172=VECTOR('',#7539,0.7);
#2173=VECTOR('',#7544,0.75);
#2174=VECTOR('',#7551,0.7);
#2604=VERTEX_POINT('',#9642);
#2605=VERTEX_POINT('',#9644);
#2606=VERTEX_POINT('',#9648);
#2607=VERTEX_POINT('',#9653);
#3305=EDGE_CURVE('',#2604,#2604,#497,.T.);
#3306=EDGE_CURVE('',#2604,#2605,#1710,.T.);
#3307=EDGE_CURVE('',#2605,#2605,#498,.T.);
#3308=EDGE_CURVE('',#2605,#2606,#1711,.T.);
#3309=EDGE_CURVE('',#2606,#2606,#499,.T.);
#3310=EDGE_CURVE('',#2606,#2607,#1712,.T.);
#3311=EDGE_CURVE('',#2607,#2607,#500,.T.);
#4680=ORIENTED_EDGE('',*,*,#3305,.F.);
#4681=ORIENTED_EDGE('',*,*,#3306,.T.);
#4682=ORIENTED_EDGE('',*,*,#3307,.F.);
#4683=ORIENTED_EDGE('',*,*,#3306,.F.);
#4684=ORIENTED_EDGE('',*,*,#3307,.T.);
#4685=ORIENTED_EDGE('',*,*,#3308,.T.);
#4686=ORIENTED_EDGE('',*,*,#3309,.T.);
#4687=ORIENTED_EDGE('',*,*,#3308,.F.);
#4688=ORIENTED_EDGE('',*,*,#3305,.T.);
#4689=ORIENTED_EDGE('',*,*,#3309,.F.);
#4690=ORIENTED_EDGE('',*,*,#3310,.T.);
#4691=ORIENTED_EDGE('',*,*,#3311,.F.);
#4692=ORIENTED_EDGE('',*,*,#3310,.F.);
#4693=ORIENTED_EDGE('',*,*,#3311,.T.);
#4989=PLANE('',#6010);
#4990=PLANE('',#6013);
#5292=ADVANCED_FACE('',(#880),#265,.T.);
#5293=ADVANCED_FACE('',(#881),#599,.T.);
#5294=ADVANCED_FACE('',(#882),#4989,.F.);
#5295=ADVANCED_FACE('',(#883),#266,.T.);
#5296=ADVANCED_FACE('',(#884),#4990,.T.);
#5347=CLOSED_SHELL('',(#5292,#5293,#5294,#5295,#5296));
#6004=AXIS2_PLACEMENT_3D('',#9640,#7533,#7534);
#6005=AXIS2_PLACEMENT_3D('',#9641,#7535,#7536);
#6006=AXIS2_PLACEMENT_3D('',#9643,#7537,#7538);
#6007=AXIS2_PLACEMENT_3D('',#9646,#7540,#7541);
#6008=AXIS2_PLACEMENT_3D('',#9647,#7542,#7543);
#6009=AXIS2_PLACEMENT_3D('',#9650,#7545,#7546);
#6010=AXIS2_PLACEMENT_3D('',#9651,#7547,#7548);
#6011=AXIS2_PLACEMENT_3D('',#9652,#7549,#7550);
#6012=AXIS2_PLACEMENT_3D('',#9655,#7552,#7553);
#6013=AXIS2_PLACEMENT_3D('',#9656,#7554,#7555);
#7533=DIRECTION('axis',(0.,0.,1.));
#7534=DIRECTION('refdir',(1.,0.,0.));
#7535=DIRECTION('center_axis',(2.22044604925031E-16,-1.,-1.22464679914735E-16));
#7536=DIRECTION('ref_axis',(-1.,-2.22044604925031E-16,-2.71926214689378E-32));
#7537=DIRECTION('center_axis',(-2.22044604925031E-16,1.,1.22464679914735E-16));
#7538=DIRECTION('ref_axis',(-1.,-2.22044604925031E-16,-2.71926214689378E-32));
#7539=DIRECTION('',(0.70710678118655,-0.707106781186545,4.95239128556718E-31));
#7540=DIRECTION('center_axis',(2.22044604925031E-16,-1.,-1.22464679914735E-16));
#7541=DIRECTION('ref_axis',(-1.,-2.22044604925031E-16,-2.71926214689378E-32));
#7542=DIRECTION('center_axis',(2.22044604925031E-16,-1.,-1.22464679914735E-16));
#7543=DIRECTION('ref_axis',(-1.,-2.22044604925031E-16,-2.71926214689378E-32));
#7544=DIRECTION('',(2.22044604925031E-16,-1.,-1.22464679914735E-16));
#7545=DIRECTION('center_axis',(-2.22044604925031E-16,1.,1.22464679914735E-16));
#7546=DIRECTION('ref_axis',(-1.,-2.22044604925031E-16,-2.71926214689378E-32));
#7547=DIRECTION('center_axis',(2.22044604925031E-16,-1.,-1.22464679914735E-16));
#7548=DIRECTION('ref_axis',(0.,-1.22464679914735E-16,1.));
#7549=DIRECTION('center_axis',(-2.22044604925031E-16,1.,1.22464679914735E-16));
#7550=DIRECTION('ref_axis',(-1.,-2.22044604925031E-16,-2.71926214689378E-32));
#7551=DIRECTION('',(-0.707106781186547,-0.707106781186548,-1.73191211247099E-16));
#7552=DIRECTION('center_axis',(2.22044604925031E-16,-1.,-1.22464679914735E-16));
#7553=DIRECTION('ref_axis',(-1.,-2.22044604925031E-16,-2.71926214689378E-32));
#7554=DIRECTION('center_axis',(2.22044604925031E-16,-1.,-1.22464679914735E-16));
#7555=DIRECTION('ref_axis',(0.,-1.22464679914735E-16,1.));
#9640=CARTESIAN_POINT('',(0.,0.,0.));
#9641=CARTESIAN_POINT('Origin',(-10.9359120418715,27.7504782148047,17.6));
#9642=CARTESIAN_POINT('',(-10.2859120418715,27.8004782148047,17.6));
#9643=CARTESIAN_POINT('Origin',(-10.9359120418715,27.8004782148047,17.6));
#9644=CARTESIAN_POINT('',(-10.1859120418715,27.7004782148047,17.6));
#9645=CARTESIAN_POINT('',(-10.2359120418715,27.7504782148047,17.6));
#9646=CARTESIAN_POINT('Origin',(-10.9359120418715,27.7004782148047,17.6));
#9647=CARTESIAN_POINT('Origin',(-10.9359120418715,22.4004782148047,17.6));
#9648=CARTESIAN_POINT('',(-10.1859120418715,22.5004782148047,17.6));
#9649=CARTESIAN_POINT('',(-10.1859120418715,22.4004782148047,17.6));
#9650=CARTESIAN_POINT('Origin',(-10.9359120418715,22.5004782148047,17.6));
#9651=CARTESIAN_POINT('Origin',(-10.9359120418715,27.8004782148047,17.6));
#9652=CARTESIAN_POINT('Origin',(-10.9359120418715,22.4504782148047,17.6));
#9653=CARTESIAN_POINT('',(-10.2859120418715,22.4004782148047,17.6));
#9654=CARTESIAN_POINT('',(-10.2359120418715,22.4504782148047,17.6));
#9655=CARTESIAN_POINT('Origin',(-10.9359120418715,22.4004782148047,17.6));
#9656=CARTESIAN_POINT('Origin',(-10.9359120418715,22.4004782148047,17.6));
#11362=UNCERTAINTY_MEASURE_WITH_UNIT(LENGTH_MEASURE(0.01),#11386,
'DISTANCE_ACCURACY_VALUE',
'Maximum model space distance between geometric entities at asserted c
onnectivities');
#11370=UNCERTAINTY_MEASURE_WITH_UNIT(LENGTH_MEASURE(0.01),#11386,
'DISTANCE_ACCURACY_VALUE',
'Maximum model space distance between geometric entities at asserted c
onnectivities');
#11377=(
GEOMETRIC_REPRESENTATION_CONTEXT(3)
GLOBAL_UNCERTAINTY_ASSIGNED_CONTEXT((#11362))
GLOBAL_UNIT_ASSIGNED_CONTEXT((#11386,#11388,#11389))
REPRESENTATION_CONTEXT('','3D')
);
#11385=(
GEOMETRIC_REPRESENTATION_CONTEXT(3)
GLOBAL_UNCERTAINTY_ASSIGNED_CONTEXT((#11370))
GLOBAL_UNIT_ASSIGNED_CONTEXT((#11386,#11388,#11389))
REPRESENTATION_CONTEXT('','3D')
);
#11386=(
LENGTH_UNIT()
NAMED_UNIT(*)
SI_UNIT(.MILLI.,.METRE.)
);
#11388=(
NAMED_UNIT(*)
PLANE_ANGLE_UNIT()
SI_UNIT($,.RADIAN.)
);
#11389=(
NAMED_UNIT(*)
SI_UNIT($,.STERADIAN.)
SOLID_ANGLE_UNIT()
);
#11396=SHAPE_DEFINITION_REPRESENTATION(#11410,#11437);
#11410=PRODUCT_DEFINITION_SHAPE('',$,#11452);
#11437=SHAPE_REPRESENTATION('',(#6004),#11377);
#11445=PRODUCT_DEFINITION_CONTEXT('part definition',#11489,'design');
#11452=PRODUCT_DEFINITION('Pin_04','Pin_04',#11466,#11445);
#11466=PRODUCT_DEFINITION_FORMATION('',$,#11497);
#11489=APPLICATION_CONTEXT(
'Core Data for Automotive Mechanical Design Process');
#11490=PRODUCT_CONTEXT('part definition',#11489,'mechanical');
#11497=PRODUCT('Pin_04','Pin_04',$,(#11490));
#11561=COLOUR_RGB('Grey',0.48,0.52,0.57);
#11562=FILL_AREA_STYLE_COLOUR('',#11561);
#11563=FILL_AREA_STYLE('',(#11562));
#11564=SURFACE_STYLE_FILL_AREA(#11563);
#11565=SURFACE_SIDE_STYLE('',(#11564));
#11566=SURFACE_STYLE_USAGE(.BOTH.,#11565);
#11567=PRESENTATION_STYLE_ASSIGNMENT((#11566));
ENDSEC;
END-ISO-10303-21;
